ISO-10303-21;
HEADER;
FILE_DESCRIPTION (('STEP AP214'),
    '1' );
FILE_NAME ('5. Handle.step',
    '2026-10-09T08:13:37',
    ( '' ),
    ( '' ),
    'SwSTEP 2.0',
    'SolidWorks 2021',
    '' );
FILE_SCHEMA (( 'AUTOMOTIVE_DESIGN' ));
ENDSEC;

DATA;
#601=AXIS2_PLACEMENT_3D ( 'NONE', #12597, #1301, #1663 ) ;
#730=FILL_AREA_STYLE ('',( #12736 ) ) ;
#783=ADVANCED_FACE ( 'NONE', ( #49924 ), #48915, .T. ) ;
#1071=( NAMED_UNIT ( * ) PLANE_ANGLE_UNIT ( ) SI_UNIT ( $, .RADIAN. ) );
#1169=AXIS2_PLACEMENT_3D ( 'NONE', #11637, #23568, #65083 ) ;
#1204=DIRECTION ( 'NONE',  ( 1.000000000000000000, 0.000000000000000000, 0.000000000000000000 ) ) ;
#1288=DIRECTION ( 'NONE',  ( 0.000000000000000000, 1.000000000000000000, 0.000000000000000000 ) ) ;
#1301=DIRECTION ( 'NONE',  ( -0.000000000000000000, 0.000000000000000000, -1.000000000000000000 ) ) ;
#1663=DIRECTION ( 'NONE',  ( 0.000000000000000000, 1.000000000000000000, 0.000000000000000000 ) ) ;
#2208=SHAPE_DEFINITION_REPRESENTATION ( #19788, #14558 ) ;
#2290=MECHANICAL_DESIGN_GEOMETRIC_PRESENTATION_REPRESENTATION('',(#46249),#23713);
#2784=ORIENTED_EDGE ( 'NONE', *, *, #31129, .F. ) ;
#2998=UNCERTAINTY_MEASURE_WITH_UNIT (LENGTH_MEASURE( 1.000000000000000082E-05 ), #60919, 'distance_accuracy_value', 'NONE');
#3068=VERTEX_POINT ( 'NONE', #17890 ) ;
#3163=DIRECTION ( 'NONE',  ( 0.000000000000000000, 0.000000000000000000, 1.000000000000000000 ) ) ;
#3448=FACE_OUTER_BOUND ( 'NONE', #28034, .T. ) ;
#3804=DIRECTION ( 'NONE',  ( -1.000000000000000000, -0.000000000000000000, -0.000000000000000000 ) ) ;
#4589=FILL_AREA_STYLE ('',( #47929 ) ) ;
#4838=DIRECTION ( 'NONE',  ( 0.000000000000000000, 0.000000000000000000, 1.000000000000000000 ) ) ;
#5115=CARTESIAN_POINT ( 'NONE',  ( 179.4098300562505415, -5.000000000000010658, -6.123233995736778115E-16 ) ) ;
#5161=EDGE_LOOP ( 'NONE', ( #59188, #43424, #36157, #18899, #34260, #67235 ) ) ;
#6562=VERTEX_POINT ( 'NONE', #20395 ) ;
#6708=CARTESIAN_POINT ( 'NONE',  ( 179.4098300562505415, 0.000000000000000000, 0.000000000000000000 ) ) ;
#6763=( NAMED_UNIT ( * ) SI_UNIT ( $, .STERADIAN. ) SOLID_ANGLE_UNIT ( ) );
#6839=CARTESIAN_POINT ( 'NONE',  ( 179.4098300562505415, 0.000000000000000000, 0.000000000000000000 ) ) ;
#6858=VECTOR ( 'NONE', #43595, 1000.000000000000000 ) ;
#7070=DIRECTION ( 'NONE',  ( -1.000000000000000000, -0.000000000000000000, -0.000000000000000000 ) ) ;
#7217=DIRECTION ( 'NONE',  ( 0.000000000000000000, 0.000000000000000000, 1.000000000000000000 ) ) ;
#7501=UNCERTAINTY_MEASURE_WITH_UNIT (LENGTH_MEASURE( 1.000000000000000082E-05 ), #9904, 'distance_accuracy_value', 'NONE');
#8211=DIRECTION ( 'NONE',  ( -0.000000000000000000, 0.000000000000000000, 1.000000000000000000 ) ) ;
#8869=AXIS2_PLACEMENT_3D ( 'NONE', #36914, #10836, #63265 ) ;
#9447=DIRECTION ( 'NONE',  ( 0.000000000000000000, 0.000000000000000000, 1.000000000000000000 ) ) ;
#9794=CARTESIAN_POINT ( 'NONE',  ( 5.590169943749474513, 4.999999999999999112, 0.000000000000000000 ) ) ;
#9904=( LENGTH_UNIT ( ) NAMED_UNIT ( * ) SI_UNIT ( .MILLI., .METRE. ) );
#10009=VERTEX_POINT ( 'NONE', #56642 ) ;
#10057=DIRECTION ( 'NONE',  ( 0.000000000000000000, 0.000000000000000000, 1.000000000000000000 ) ) ;
#10836=DIRECTION ( 'NONE',  ( 0.000000000000000000, 1.224646799147353207E-16, -1.000000000000000000 ) ) ;
#11523=CLOSED_SHELL ( 'NONE', ( #21668, #23996, #783, #17496, #62733, #57184 ) ) ;
#11637=CARTESIAN_POINT ( 'NONE',  ( 0.000000000000000000, 0.000000000000000000, 0.000000000000000000 ) ) ;
#11708=SURFACE_STYLE_FILL_AREA ( #730 ) ;
#12560=DIRECTION ( 'NONE',  ( -1.000000000000000000, -0.000000000000000000, -0.000000000000000000 ) ) ;
#12597=CARTESIAN_POINT ( 'NONE',  ( 185.0000000000000000, 0.000000000000000000, 0.000000000000000000 ) ) ;
#12736=FILL_AREA_STYLE_COLOUR ( '', #51852 ) ;
#12849=( GEOMETRIC_REPRESENTATION_CONTEXT ( 3 ) GLOBAL_UNCERTAINTY_ASSIGNED_CONTEXT ( ( #7501 ) ) GLOBAL_UNIT_ASSIGNED_CONTEXT ( ( #9904, #42627, #64033 ) ) REPRESENTATION_CONTEXT ( 'NONE', 'WORKASPACE' ) );
#13559=EDGE_CURVE ( 'NONE', #3068, #20313, #34930, .T. ) ;
#13756=EDGE_CURVE ( 'NONE', #36746, #17595, #17855, .T. ) ;
#14102=AXIS2_PLACEMENT_3D ( 'NONE', #20102, #14868, #36352 ) ;
#14558=SHAPE_REPRESENTATION ( '5. Handle', ( #42840 ), #37272 ) ;
#14610=EDGE_LOOP ( 'NONE', ( #25393, #37395, #14866, #33039 ) ) ;
#14866=ORIENTED_EDGE ( 'NONE', *, *, #13559, .F. ) ;
#14868=DIRECTION ( 'NONE',  ( 0.000000000000000000, 1.224646799147353207E-16, -1.000000000000000000 ) ) ;
#16991=AXIS2_PLACEMENT_3D ( 'NONE', #53750, #12560, #38672 ) ;
#17006=( NAMED_UNIT ( * ) PLANE_ANGLE_UNIT ( ) SI_UNIT ( $, .RADIAN. ) );
#17496=ADVANCED_FACE ( 'NONE', ( #3448 ), #47150, .T. ) ;
#17595=VERTEX_POINT ( 'NONE', #26660 ) ;
#17699=SURFACE_SIDE_STYLE ('',( #11708 ) ) ;
#17855=LINE ( 'NONE', #32627, #6858 ) ;
#17890=CARTESIAN_POINT ( 'NONE',  ( 179.4098300562505415, 6.123233995736766282E-16, -5.000000000000000000 ) ) ;
#17959=SPHERICAL_SURFACE ( 'NONE', #1169, 7.500000000000000000 ) ;
#18061=CARTESIAN_POINT ( 'NONE',  ( 185.0000000000000000, 0.000000000000000000, 0.000000000000000000 ) ) ;
#18329=DIRECTION ( 'NONE',  ( 0.000000000000000000, 0.000000000000000000, 1.000000000000000000 ) ) ;
#18650=AXIS2_PLACEMENT_3D ( 'NONE', #18061, #8211, #29657 ) ;
#18899=ORIENTED_EDGE ( 'NONE', *, *, #28439, .F. ) ;
#18922=CARTESIAN_POINT ( 'NONE',  ( 5.590169943749474513, 0.000000000000000000, 0.000000000000000000 ) ) ;
#19788=PRODUCT_DEFINITION_SHAPE ( 'NONE', 'NONE',  #27444 ) ;
#19850=CIRCLE ( 'NONE', #64755, 7.500000000000000000 ) ;
#20102=CARTESIAN_POINT ( 'NONE',  ( 185.0000000000000000, 0.000000000000000000, 0.000000000000000000 ) ) ;
#20313=VERTEX_POINT ( 'NONE', #5115 ) ;
#20323=DIRECTION ( 'NONE',  ( -1.000000000000000000, -0.000000000000000000, -0.000000000000000000 ) ) ;
#20395=CARTESIAN_POINT ( 'NONE',  ( 192.5000000000000000, 4.592425496802570028E-16, 0.000000000000000000 ) ) ;
#20443=AXIS2_PLACEMENT_3D ( 'NONE', #18922, #20323, #9447 ) ;
#21183=CIRCLE ( 'NONE', #30153, 5.000000000000000000 ) ;
#21187=CARTESIAN_POINT ( 'NONE',  ( 179.4098300562505415, 5.000000000000010658, 0.000000000000000000 ) ) ;
#21596=EDGE_CURVE ( 'NONE', #3068, #10009, #31704, .T. ) ;
#21668=ADVANCED_FACE ( 'NONE', ( #43694 ), #17959, .T. ) ;
#22642=EDGE_CURVE ( 'NONE', #36746, #25647, #48637, .T. ) ;
#22702=AXIS2_PLACEMENT_3D ( 'NONE', #31915, #52701, #4838 ) ;
#23300=SHAPE_REPRESENTATION_RELATIONSHIP ( 'NONE' , 'NONE' ,  #14558, #41398 ) ;
#23568=DIRECTION ( 'NONE',  ( -0.000000000000000000, 0.000000000000000000, -1.000000000000000000 ) ) ;
#23713=( GEOMETRIC_REPRESENTATION_CONTEXT ( 3 ) GLOBAL_UNCERTAINTY_ASSIGNED_CONTEXT ( ( #2998 ) ) GLOBAL_UNIT_ASSIGNED_CONTEXT ( ( #60919, #1071, #6763 ) ) REPRESENTATION_CONTEXT ( 'NONE', 'WORKASPACE' ) );
#23996=ADVANCED_FACE ( 'NONE', ( #36725 ), #30325, .T. ) ;
#24828=ORIENTED_EDGE ( 'NONE', *, *, #28292, .F. ) ;
#25080=DIRECTION ( 'NONE',  ( -1.000000000000000000, -0.000000000000000000, -0.000000000000000000 ) ) ;
#25207=MECHANICAL_DESIGN_GEOMETRIC_PRESENTATION_REPRESENTATION('',(#37619),#12849);
#25383=DIRECTION ( 'NONE',  ( -1.000000000000000000, -0.000000000000000000, -0.000000000000000000 ) ) ;
#25393=ORIENTED_EDGE ( 'NONE', *, *, #49865, .F. ) ;
#25647=VERTEX_POINT ( 'NONE', #21187 ) ;
#26047=SURFACE_STYLE_FILL_AREA ( #4589 ) ;
#26172=ORIENTED_EDGE ( 'NONE', *, *, #49865, .T. ) ;
#26660=CARTESIAN_POINT ( 'NONE',  ( 5.590169943749474513, 0.000000000000000000, 4.999999999999999112 ) ) ;
#26681=VERTEX_POINT ( 'NONE', #54746 ) ;
#27198=MANIFOLD_SOLID_BREP ( 'Revolve1', #11523 ) ;
#27444=PRODUCT_DEFINITION ( 'UNKNOWN', '', #32630, #53662 ) ;
#28034=EDGE_LOOP ( 'NONE', ( #59089, #26172, #47612, #35823 ) ) ;
#28292=EDGE_CURVE ( 'NONE', #10009, #45103, #60840, .T. ) ;
#28439=EDGE_CURVE ( 'NONE', #17595, #62740, #46286, .T. ) ;
#29277=CARTESIAN_POINT ( 'NONE',  ( 5.590169943749474513, -4.999999999999999112, -6.123233995736765296E-16 ) ) ;
#29280=ORIENTED_EDGE ( 'NONE', *, *, #13559, .T. ) ;
#29657=DIRECTION ( 'NONE',  ( 1.000000000000000000, 0.000000000000000000, 0.000000000000000000 ) ) ;
#29795=UNCERTAINTY_MEASURE_WITH_UNIT (LENGTH_MEASURE( 1.000000000000000082E-05 ), #31771, 'distance_accuracy_value', 'NONE');
#29857=AXIS2_PLACEMENT_3D ( 'NONE', #43964, #33028, #1288 ) ;
#30071=EDGE_LOOP ( 'NONE', ( #46833, #29280, #40657, #40030, #2784, #24828 ) ) ;
#30153=AXIS2_PLACEMENT_3D ( 'NONE', #6839, #48767, #44185 ) ;
#30325=CYLINDRICAL_SURFACE ( 'NONE', #56395, 4.999999999999999112 ) ;
#30624=SURFACE_STYLE_USAGE ( .BOTH. , #37008 ) ;
#30756=CIRCLE ( 'NONE', #66729, 4.999999999999999112 ) ;
#31129=EDGE_CURVE ( 'NONE', #45103, #17595, #30756, .T. ) ;
#31345=CIRCLE ( 'NONE', #51550, 4.999999999999999112 ) ;
#31470=AXIS2_PLACEMENT_3D ( 'NONE', #40465, #61885, #62918 ) ;
#31704=LINE ( 'NONE', #53184, #60766 ) ;
#31771=( LENGTH_UNIT ( ) NAMED_UNIT ( * ) SI_UNIT ( .MILLI., .METRE. ) );
#31915=CARTESIAN_POINT ( 'NONE',  ( 5.590169943749474513, 0.000000000000000000, 0.000000000000000000 ) ) ;
#32009=EDGE_LOOP ( 'NONE', ( #39099, #38793, #65389, #66957 ) ) ;
#32627=CARTESIAN_POINT ( 'NONE',  ( -7.499999999999999112, 0.000000000000000000, 4.999999999999999112 ) ) ;
#32630=PRODUCT_DEFINITION_FORMATION_WITH_SPECIFIED_SOURCE ( 'ANY', '', #32768, .NOT_KNOWN. ) ;
#32768=PRODUCT ( '5. Handle', '5. Handle', '', ( #60660 ) ) ;
#33028=DIRECTION ( 'NONE',  ( -0.000000000000000000, 0.000000000000000000, -1.000000000000000000 ) ) ;
#33039=ORIENTED_EDGE ( 'NONE', *, *, #66382, .F. ) ;
#33505=PRESENTATION_STYLE_ASSIGNMENT (( #50057 ) ) ;
#34260=ORIENTED_EDGE ( 'NONE', *, *, #13756, .F. ) ;
#34363=CIRCLE ( 'NONE', #18650, 7.500000000000007105 ) ;
#34930=CIRCLE ( 'NONE', #55137, 5.000000000000000000 ) ;
#35155=CARTESIAN_POINT ( 'NONE',  ( 179.4098300562505415, 0.000000000000000000, 0.000000000000000000 ) ) ;
#35318=COLOUR_RGB ( '', 0.66274510, 0.83137255, 0.94901961) ;
#35823=ORIENTED_EDGE ( 'NONE', *, *, #53659, .F. ) ;
#35852=DIRECTION ( 'NONE',  ( 0.000000000000000000, 0.000000000000000000, 1.000000000000000000 ) ) ;
#36157=ORIENTED_EDGE ( 'NONE', *, *, #42530, .F. ) ;
#36352=DIRECTION ( 'NONE',  ( 0.000000000000000000, 1.000000000000000000, 1.224646799147353207E-16 ) ) ;
#36725=FACE_OUTER_BOUND ( 'NONE', #5161, .T. ) ;
#36746=VERTEX_POINT ( 'NONE', #38626 ) ;
#36914=CARTESIAN_POINT ( 'NONE',  ( 0.000000000000000000, 0.000000000000000000, 0.000000000000000000 ) ) ;
#37008=SURFACE_SIDE_STYLE ('',( #26047 ) ) ;
#37272=( GEOMETRIC_REPRESENTATION_CONTEXT ( 3 ) GLOBAL_UNCERTAINTY_ASSIGNED_CONTEXT ( ( #29795 ) ) GLOBAL_UNIT_ASSIGNED_CONTEXT ( ( #31771, #17006, #44465 ) ) REPRESENTATION_CONTEXT ( 'NONE', 'WORKASPACE' ) );
#37395=ORIENTED_EDGE ( 'NONE', *, *, #39111, .T. ) ;
#37619=STYLED_ITEM ( 'NONE', ( #52131 ), #27198 ) ;
#37746=CIRCLE ( 'NONE', #14102, 7.499999999999992895 ) ;
#38626=CARTESIAN_POINT ( 'NONE',  ( 179.4098300562505415, 0.000000000000000000, 5.000000000000000000 ) ) ;
#38672=DIRECTION ( 'NONE',  ( 0.000000000000000000, 0.000000000000000000, 1.000000000000000000 ) ) ;
#38793=ORIENTED_EDGE ( 'NONE', *, *, #43590, .T. ) ;
#39099=ORIENTED_EDGE ( 'NONE', *, *, #28292, .T. ) ;
#39111=EDGE_CURVE ( 'NONE', #6562, #20313, #37746, .T. ) ;
#40030=ORIENTED_EDGE ( 'NONE', *, *, #13756, .T. ) ;
#40209=EDGE_CURVE ( 'NONE', #62740, #26681, #19850, .T. ) ;
#40465=CARTESIAN_POINT ( 'NONE',  ( 185.0000000000000000, 0.000000000000000000, 0.000000000000000000 ) ) ;
#40657=ORIENTED_EDGE ( 'NONE', *, *, #53659, .T. ) ;
#41398=ADVANCED_BREP_SHAPE_REPRESENTATION ( '', ( #27198, #42840 ), #37272 ) ;
#42530=EDGE_CURVE ( 'NONE', #62740, #10009, #31345, .T. ) ;
#42627=( NAMED_UNIT ( * ) PLANE_ANGLE_UNIT ( ) SI_UNIT ( $, .RADIAN. ) );
#42840=AXIS2_PLACEMENT_3D ( 'NONE', #59977, #7217, #49786 ) ;
#43424=ORIENTED_EDGE ( 'NONE', *, *, #21596, .T. ) ;
#43590=EDGE_CURVE ( 'NONE', #45103, #26681, #60512, .T. ) ;
#43595=DIRECTION ( 'NONE',  ( -1.000000000000000000, -0.000000000000000000, -0.000000000000000000 ) ) ;
#43694=FACE_OUTER_BOUND ( 'NONE', #32009, .T. ) ;
#43964=CARTESIAN_POINT ( 'NONE',  ( 0.000000000000000000, 0.000000000000000000, 0.000000000000000000 ) ) ;
#44185=DIRECTION ( 'NONE',  ( 0.000000000000000000, 0.000000000000000000, 1.000000000000000000 ) ) ;
#44465=( NAMED_UNIT ( * ) SI_UNIT ( $, .STERADIAN. ) SOLID_ANGLE_UNIT ( ) );
#44659=ORIENTED_EDGE ( 'NONE', *, *, #40209, .T. ) ;
#45103=VERTEX_POINT ( 'NONE', #29277 ) ;
#46249=STYLED_ITEM ( 'NONE', ( #33505 ), #41398 ) ;
#46286=CIRCLE ( 'NONE', #22702, 4.999999999999999112 ) ;
#46833=ORIENTED_EDGE ( 'NONE', *, *, #21596, .F. ) ;
#47101=CARTESIAN_POINT ( 'NONE',  ( -7.499999999999999112, 0.000000000000000000, 0.000000000000000000 ) ) ;
#47150=SPHERICAL_SURFACE ( 'NONE', #31470, 7.499999999999992895 ) ;
#47461=CYLINDRICAL_SURFACE ( 'NONE', #47683, 4.999999999999999112 ) ;
#47612=ORIENTED_EDGE ( 'NONE', *, *, #22642, .F. ) ;
#47683=AXIS2_PLACEMENT_3D ( 'NONE', #47101, #68523, #58306 ) ;
#47929=FILL_AREA_STYLE_COLOUR ( '', #35318 ) ;
#48637=CIRCLE ( 'NONE', #68837, 5.000000000000000000 ) ;
#48767=DIRECTION ( 'NONE',  ( -1.000000000000000000, -0.000000000000000000, -0.000000000000000000 ) ) ;
#48915=SPHERICAL_SURFACE ( 'NONE', #601, 7.499999999999992895 ) ;
#49558=SPHERICAL_SURFACE ( 'NONE', #29857, 7.500000000000000000 ) ;
#49786=DIRECTION ( 'NONE',  ( 1.000000000000000000, 0.000000000000000000, 0.000000000000000000 ) ) ;
#49825=ORIENTED_EDGE ( 'NONE', *, *, #28439, .T. ) ;
#49865=EDGE_CURVE ( 'NONE', #6562, #25647, #34363, .T. ) ;
#49924=FACE_OUTER_BOUND ( 'NONE', #14610, .T. ) ;
#49993=ORIENTED_EDGE ( 'NONE', *, *, #43590, .F. ) ;
#50057=SURFACE_STYLE_USAGE ( .BOTH. , #17699 ) ;
#51550=AXIS2_PLACEMENT_3D ( 'NONE', #63510, #58233, #10057 ) ;
#51826=CARTESIAN_POINT ( 'NONE',  ( -7.499999999999999112, 0.000000000000000000, 0.000000000000000000 ) ) ;
#51852=COLOUR_RGB ( '', 0.66274510, 0.83137255, 0.94901961) ;
#52131=PRESENTATION_STYLE_ASSIGNMENT (( #30624 ) ) ;
#52151=CARTESIAN_POINT ( 'NONE',  ( 5.590169943749474513, 0.000000000000000000, 0.000000000000000000 ) ) ;
#52367=FACE_OUTER_BOUND ( 'NONE', #30071, .T. ) ;
#52701=DIRECTION ( 'NONE',  ( -1.000000000000000000, -0.000000000000000000, -0.000000000000000000 ) ) ;
#52753=APPLICATION_CONTEXT ( 'automotive_design' ) ;
#53184=CARTESIAN_POINT ( 'NONE',  ( -7.499999999999999112, 6.123233995736765296E-16, -4.999999999999999112 ) ) ;
#53659=EDGE_CURVE ( 'NONE', #20313, #36746, #67526, .T. ) ;
#53662=PRODUCT_DEFINITION_CONTEXT ( 'detailed design', #52753, 'design' ) ;
#53750=CARTESIAN_POINT ( 'NONE',  ( 179.4098300562505415, 0.000000000000000000, 0.000000000000000000 ) ) ;
#54032=DIRECTION ( 'NONE',  ( -0.000000000000000000, 0.000000000000000000, 1.000000000000000000 ) ) ;
#54746=CARTESIAN_POINT ( 'NONE',  ( -7.500000000000000000, 4.592425496802573972E-16, 0.000000000000000000 ) ) ;
#55063=CARTESIAN_POINT ( 'NONE',  ( 0.000000000000000000, 0.000000000000000000, 0.000000000000000000 ) ) ;
#55137=AXIS2_PLACEMENT_3D ( 'NONE', #35155, #3804, #35852 ) ;
#56395=AXIS2_PLACEMENT_3D ( 'NONE', #51826, #25080, #68011 ) ;
#56642=CARTESIAN_POINT ( 'NONE',  ( 5.590169943749474513, 6.123233995736765296E-16, -4.999999999999999112 ) ) ;
#57184=ADVANCED_FACE ( 'NONE', ( #60093 ), #49558, .T. ) ;
#57672=APPLICATION_CONTEXT ( 'automotive_design' ) ;
#58233=DIRECTION ( 'NONE',  ( -1.000000000000000000, -0.000000000000000000, -0.000000000000000000 ) ) ;
#58306=DIRECTION ( 'NONE',  ( 0.000000000000000000, 0.000000000000000000, 1.000000000000000000 ) ) ;
#59089=ORIENTED_EDGE ( 'NONE', *, *, #39111, .F. ) ;
#59188=ORIENTED_EDGE ( 'NONE', *, *, #66382, .T. ) ;
#59977=CARTESIAN_POINT ( 'NONE',  ( 0.000000000000000000, 0.000000000000000000, 0.000000000000000000 ) ) ;
#60093=FACE_OUTER_BOUND ( 'NONE', #68582, .T. ) ;
#60512=CIRCLE ( 'NONE', #8869, 7.500000000000000000 ) ;
#60660=PRODUCT_CONTEXT ( 'NONE', #57672, 'mechanical' ) ;
#60766=VECTOR ( 'NONE', #69353, 1000.000000000000000 ) ;
#60840=CIRCLE ( 'NONE', #20443, 4.999999999999999112 ) ;
#60919=( LENGTH_UNIT ( ) NAMED_UNIT ( * ) SI_UNIT ( .MILLI., .METRE. ) );
#61885=DIRECTION ( 'NONE',  ( -0.000000000000000000, 0.000000000000000000, -1.000000000000000000 ) ) ;
#62733=ADVANCED_FACE ( 'NONE', ( #52367 ), #47461, .T. ) ;
#62740=VERTEX_POINT ( 'NONE', #9794 ) ;
#62918=DIRECTION ( 'NONE',  ( 0.000000000000000000, 1.000000000000000000, 0.000000000000000000 ) ) ;
#63265=DIRECTION ( 'NONE',  ( 0.000000000000000000, 1.000000000000000000, 1.224646799147352961E-16 ) ) ;
#63510=CARTESIAN_POINT ( 'NONE',  ( 5.590169943749474513, 0.000000000000000000, 0.000000000000000000 ) ) ;
#64033=( NAMED_UNIT ( * ) SI_UNIT ( $, .STERADIAN. ) SOLID_ANGLE_UNIT ( ) );
#64755=AXIS2_PLACEMENT_3D ( 'NONE', #55063, #54032, #1204 ) ;
#65083=DIRECTION ( 'NONE',  ( 0.000000000000000000, 1.000000000000000000, 0.000000000000000000 ) ) ;
#65389=ORIENTED_EDGE ( 'NONE', *, *, #40209, .F. ) ;
#66382=EDGE_CURVE ( 'NONE', #25647, #3068, #21183, .T. ) ;
#66729=AXIS2_PLACEMENT_3D ( 'NONE', #52151, #25383, #3163 ) ;
#66957=ORIENTED_EDGE ( 'NONE', *, *, #42530, .T. ) ;
#67235=ORIENTED_EDGE ( 'NONE', *, *, #22642, .T. ) ;
#67526=CIRCLE ( 'NONE', #16991, 5.000000000000000000 ) ;
#67806=ORIENTED_EDGE ( 'NONE', *, *, #31129, .T. ) ;
#68011=DIRECTION ( 'NONE',  ( 0.000000000000000000, 0.000000000000000000, 1.000000000000000000 ) ) ;
#68523=DIRECTION ( 'NONE',  ( -1.000000000000000000, -0.000000000000000000, -0.000000000000000000 ) ) ;
#68582=EDGE_LOOP ( 'NONE', ( #49993, #67806, #49825, #44659 ) ) ;
#68837=AXIS2_PLACEMENT_3D ( 'NONE', #6708, #7070, #18329 ) ;
#69353=DIRECTION ( 'NONE',  ( -1.000000000000000000, -0.000000000000000000, -0.000000000000000000 ) ) ;
ENDSEC;
END-ISO-10303-21;
